ISO-10303-21;
HEADER;
/* Generated by software containing ST-Developer
 * from STEP Tools, Inc. (www.steptools.com) 
 */

FILE_DESCRIPTION(
/* description */ (''),
/* implementation_level */ '2;1');

FILE_NAME(
/* name */ 'Ball_01.step',
/* time_stamp */ '2026-10-04T23:23:09-07:00',
/* author */ (''),
/* organization */ (''),
/* preprocessor_version */ 'ST-DEVELOPER v20.2',
/* originating_system */ 'Autodesk Translation Framework v15.15.0.0',
/* authorisation */ '');

FILE_SCHEMA (('AUTOMOTIVE_DESIGN { 1 0 10303 214 3 1 1 }'));
ENDSEC;

DATA;
#10=MECHANICAL_DESIGN_GEOMETRIC_PRESENTATION_REPRESENTATION('',(#72),#2676);
#46=SPHERICAL_SURFACE('',#1706,1.);
#53=SHAPE_REPRESENTATION_RELATIONSHIP('SRR','None',#2712,#61);
#61=ADVANCED_BREP_SHAPE_REPRESENTATION('',(#83),#2672);
#72=STYLED_ITEM('',(#2757),#83);
#83=MANIFOLD_SOLID_BREP('Body1',#1483);
#252=FACE_OUTER_BOUND('',#370,.T.);
#370=EDGE_LOOP('',(#1214,#1215));
#688=CIRCLE('',#1707,1.);
#769=VERTEX_POINT('',#2493);
#770=VERTEX_POINT('',#2494);
#925=EDGE_CURVE('',#769,#770,#688,.T.);
#1214=ORIENTED_EDGE('',*,*,#925,.T.);
#1215=ORIENTED_EDGE('',*,*,#925,.F.);
#1443=ADVANCED_FACE('',(#252),#46,.T.);
#1483=CLOSED_SHELL('',(#1443));
#1705=AXIS2_PLACEMENT_3D('',#2491,#2069,#2070);
#1706=AXIS2_PLACEMENT_3D('',#2492,#2071,#2072);
#1707=AXIS2_PLACEMENT_3D('',#2495,#2073,#2074);
#2069=DIRECTION('axis',(0.,0.,1.));
#2070=DIRECTION('refdir',(1.,0.,0.));
#2071=DIRECTION('center_axis',(0.,0.,1.));
#2072=DIRECTION('ref_axis',(1.,0.,0.));
#2073=DIRECTION('center_axis',(0.,-1.,0.));
#2074=DIRECTION('ref_axis',(-1.,0.,0.));
#2491=CARTESIAN_POINT('',(0.,0.,0.));
#2492=CARTESIAN_POINT('Origin',(8.,7.5,4.));
#2493=CARTESIAN_POINT('',(8.,7.5,5.));
#2494=CARTESIAN_POINT('',(8.,7.5,3.));
#2495=CARTESIAN_POINT('Origin',(8.,7.5,4.));
#2662=UNCERTAINTY_MEASURE_WITH_UNIT(LENGTH_MEASURE(0.01),#2677,
'DISTANCE_ACCURACY_VALUE',
'Maximum model space distance between geometric entities at asserted c
onnectivities');
#2666=UNCERTAINTY_MEASURE_WITH_UNIT(LENGTH_MEASURE(0.01),#2677,
'DISTANCE_ACCURACY_VALUE',
'Maximum model space distance between geometric entities at asserted c
onnectivities');
#2672=(
GEOMETRIC_REPRESENTATION_CONTEXT(3)
GLOBAL_UNCERTAINTY_ASSIGNED_CONTEXT((#2662))
GLOBAL_UNIT_ASSIGNED_CONTEXT((#2677,#2679,#2680))
REPRESENTATION_CONTEXT('','3D')
);
#2676=(
GEOMETRIC_REPRESENTATION_CONTEXT(3)
GLOBAL_UNCERTAINTY_ASSIGNED_CONTEXT((#2666))
GLOBAL_UNIT_ASSIGNED_CONTEXT((#2677,#2679,#2680))
REPRESENTATION_CONTEXT('','3D')
);
#2677=(
LENGTH_UNIT()
NAMED_UNIT(*)
SI_UNIT(.MILLI.,.METRE.)
);
#2679=(
NAMED_UNIT(*)
PLANE_ANGLE_UNIT()
SI_UNIT($,.RADIAN.)
);
#2680=(
NAMED_UNIT(*)
SI_UNIT($,.STERADIAN.)
SOLID_ANGLE_UNIT()
);
#2686=SHAPE_DEFINITION_REPRESENTATION(#2695,#2712);
#2695=PRODUCT_DEFINITION_SHAPE('',$,#2722);
#2712=SHAPE_REPRESENTATION('',(#1705),#2672);
#2716=PRODUCT_DEFINITION_CONTEXT('part definition',#2745,'design');
#2722=PRODUCT_DEFINITION('Ball_01','Ball_01',#2731,#2716);
#2731=PRODUCT_DEFINITION_FORMATION('',$,#2752);
#2745=APPLICATION_CONTEXT(
'Core Data for Automotive Mechanical Design Process');
#2746=PRODUCT_CONTEXT('part definition',#2745,'mechanical');
#2752=PRODUCT('Ball_01','Ball_01',$,(#2746));
#2757=PRESENTATION_STYLE_ASSIGNMENT((#2759));
#2759=SURFACE_STYLE_USAGE(.BOTH.,#2761);
#2761=SURFACE_SIDE_STYLE('',(#2763));
#2763=SURFACE_STYLE_FILL_AREA(#2765);
#2765=FILL_AREA_STYLE('Opaque(203,203,203)',(#2767));
#2767=FILL_AREA_STYLE_COLOUR('Opaque(203,203,203)',#2769);
#2769=COLOUR_RGB('Opaque(203,203,203)', 0.09019608, 0.27058824, 0.51372549);
ENDSEC;
END-ISO-10303-21;
